ISO-10303-21;
HEADER;
/* Generated by software containing ST-Developer
 * from STEP Tools, Inc. (www.steptools.com) 
 */

FILE_DESCRIPTION(
/* description */ ('PAT-122'),
/* implementation_level */ '2;1');

FILE_NAME(
/* name */ 'Bonded foot pad (1).step',
/* time_stamp */ '2026-10-29T20:20:12-07:00',
/* author */ (''),
/* organization */ (''),
/* preprocessor_version */ 'ST-DEVELOPER v20.2',
/* originating_system */ 'Autodesk Translation Framework v15.17.0.0',
/* authorisation */ '');

FILE_SCHEMA (('AUTOMOTIVE_DESIGN { 1 0 10303 214 3 1 1 }'));
ENDSEC;

DATA;
#10=MECHANICAL_DESIGN_GEOMETRIC_PRESENTATION_REPRESENTATION('',(#494),#10019);
#450=SHAPE_REPRESENTATION_RELATIONSHIP('SRR','None',#10171,#472);
#472=ADVANCED_BREP_SHAPE_REPRESENTATION('',(#516),#10000);
#494=STYLED_ITEM('',(#10341),#516);
#516=MANIFOLD_SOLID_BREP('Body1',#5616);
#537=FACE_BOUND('',#1138,.T.);
#538=FACE_BOUND('',#1140,.T.);
#615=PLANE('',#5917);
#616=PLANE('',#5918);
#837=FACE_OUTER_BOUND('',#1135,.T.);
#838=FACE_OUTER_BOUND('',#1136,.T.);
#839=FACE_OUTER_BOUND('',#1137,.T.);
#840=FACE_OUTER_BOUND('',#1139,.T.);
#1135=EDGE_LOOP('',(#3901,#3902,#3903,#3904));
#1136=EDGE_LOOP('',(#3905,#3906,#3907,#3908));
#1137=EDGE_LOOP('',(#3909));
#1138=EDGE_LOOP('',(#3910));
#1139=EDGE_LOOP('',(#3911));
#1140=EDGE_LOOP('',(#3912));
#1493=LINE('',#8109,#2037);
#1494=LINE('',#8115,#2038);
#2037=VECTOR('',#6494,0.600000000000001);
#2038=VECTOR('',#6501,2.);
#2587=CIRCLE('',#5912,0.600000000000001);
#2588=CIRCLE('',#5913,0.600000000000001);
#2589=CIRCLE('',#5915,2.);
#2590=CIRCLE('',#5916,2.);
#2717=VERTEX_POINT('',#8106);
#2718=VERTEX_POINT('',#8108);
#2719=VERTEX_POINT('',#8112);
#2720=VERTEX_POINT('',#8114);
#3185=EDGE_CURVE('',#2717,#2717,#2587,.T.);
#3186=EDGE_CURVE('',#2717,#2718,#1493,.T.);
#3187=EDGE_CURVE('',#2718,#2718,#2588,.T.);
#3188=EDGE_CURVE('',#2719,#2719,#2589,.T.);
#3189=EDGE_CURVE('',#2719,#2720,#1494,.T.);
#3190=EDGE_CURVE('',#2720,#2720,#2590,.T.);
#3901=ORIENTED_EDGE('',*,*,#3185,.F.);
#3902=ORIENTED_EDGE('',*,*,#3186,.T.);
#3903=ORIENTED_EDGE('',*,*,#3187,.T.);
#3904=ORIENTED_EDGE('',*,*,#3186,.F.);
#3905=ORIENTED_EDGE('',*,*,#3188,.F.);
#3906=ORIENTED_EDGE('',*,*,#3189,.T.);
#3907=ORIENTED_EDGE('',*,*,#3190,.T.);
#3908=ORIENTED_EDGE('',*,*,#3189,.F.);
#3909=ORIENTED_EDGE('',*,*,#3188,.T.);
#3910=ORIENTED_EDGE('',*,*,#3185,.T.);
#3911=ORIENTED_EDGE('',*,*,#3190,.F.);
#3912=ORIENTED_EDGE('',*,*,#3187,.F.);
#5267=CYLINDRICAL_SURFACE('',#5911,0.600000000000001);
#5268=CYLINDRICAL_SURFACE('',#5914,2.);
#5333=ADVANCED_FACE('',(#837),#5267,.F.);
#5334=ADVANCED_FACE('',(#838),#5268,.T.);
#5335=ADVANCED_FACE('',(#839,#537),#615,.T.);
#5336=ADVANCED_FACE('',(#840,#538),#616,.F.);
#5616=CLOSED_SHELL('',(#5333,#5334,#5335,#5336));
#5910=AXIS2_PLACEMENT_3D('',#8104,#6488,#6489);
#5911=AXIS2_PLACEMENT_3D('',#8105,#6490,#6491);
#5912=AXIS2_PLACEMENT_3D('',#8107,#6492,#6493);
#5913=AXIS2_PLACEMENT_3D('',#8110,#6495,#6496);
#5914=AXIS2_PLACEMENT_3D('',#8111,#6497,#6498);
#5915=AXIS2_PLACEMENT_3D('',#8113,#6499,#6500);
#5916=AXIS2_PLACEMENT_3D('',#8116,#6502,#6503);
#5917=AXIS2_PLACEMENT_3D('',#8117,#6504,#6505);
#5918=AXIS2_PLACEMENT_3D('',#8118,#6506,#6507);
#6488=DIRECTION('axis',(0.,0.,1.));
#6489=DIRECTION('refdir',(1.,0.,0.));
#6490=DIRECTION('center_axis',(0.,0.,1.));
#6491=DIRECTION('ref_axis',(1.,0.,0.));
#6492=DIRECTION('center_axis',(0.,0.,-1.));
#6493=DIRECTION('ref_axis',(1.,0.,0.));
#6494=DIRECTION('',(0.,0.,-1.));
#6495=DIRECTION('center_axis',(0.,0.,-1.));
#6496=DIRECTION('ref_axis',(1.,0.,0.));
#6497=DIRECTION('center_axis',(0.,0.,1.));
#6498=DIRECTION('ref_axis',(1.,0.,0.));
#6499=DIRECTION('center_axis',(0.,0.,1.));
#6500=DIRECTION('ref_axis',(1.,0.,0.));
#6501=DIRECTION('',(0.,0.,-1.));
#6502=DIRECTION('center_axis',(0.,0.,1.));
#6503=DIRECTION('ref_axis',(1.,0.,0.));
#6504=DIRECTION('center_axis',(0.,0.,1.));
#6505=DIRECTION('ref_axis',(1.,0.,0.));
#6506=DIRECTION('center_axis',(0.,0.,1.));
#6507=DIRECTION('ref_axis',(1.,0.,0.));
#8104=CARTESIAN_POINT('',(0.,0.,0.));
#8105=CARTESIAN_POINT('Origin',(-19.,19.,-1.6));
#8106=CARTESIAN_POINT('',(-19.6,19.,-0.8));
#8107=CARTESIAN_POINT('Origin',(-19.,19.,-0.8));
#8108=CARTESIAN_POINT('',(-19.6,19.,-1.6));
#8109=CARTESIAN_POINT('',(-19.6,19.,-1.6));
#8110=CARTESIAN_POINT('Origin',(-19.,19.,-1.6));
#8111=CARTESIAN_POINT('Origin',(-19.,19.,-1.6));
#8112=CARTESIAN_POINT('',(-21.,19.,-0.8));
#8113=CARTESIAN_POINT('Origin',(-19.,19.,-0.8));
#8114=CARTESIAN_POINT('',(-21.,19.,-1.6));
#8115=CARTESIAN_POINT('',(-21.,19.,-1.6));
#8116=CARTESIAN_POINT('Origin',(-19.,19.,-1.6));
#8117=CARTESIAN_POINT('Origin',(-19.,19.,-0.8));
#8118=CARTESIAN_POINT('Origin',(-19.,19.,-1.6));
#9976=UNCERTAINTY_MEASURE_WITH_UNIT(LENGTH_MEASURE(0.001),#10020,
'DISTANCE_ACCURACY_VALUE',
'Maximum model space distance between geometric entities at asserted c
onnectivities');
#9995=UNCERTAINTY_MEASURE_WITH_UNIT(LENGTH_MEASURE(0.001),#10020,
'DISTANCE_ACCURACY_VALUE',
'Maximum model space distance between geometric entities at asserted c
onnectivities');
#10000=(
GEOMETRIC_REPRESENTATION_CONTEXT(3)
GLOBAL_UNCERTAINTY_ASSIGNED_CONTEXT((#9976))
GLOBAL_UNIT_ASSIGNED_CONTEXT((#10020,#10022,#10023))
REPRESENTATION_CONTEXT('','3D')
);
#10019=(
GEOMETRIC_REPRESENTATION_CONTEXT(3)
GLOBAL_UNCERTAINTY_ASSIGNED_CONTEXT((#9995))
GLOBAL_UNIT_ASSIGNED_CONTEXT((#10020,#10022,#10023))
REPRESENTATION_CONTEXT('','3D')
);
#10020=(
LENGTH_UNIT()
NAMED_UNIT(*)
SI_UNIT(.CENTI.,.METRE.)
);
#10022=(
NAMED_UNIT(*)
PLANE_ANGLE_UNIT()
SI_UNIT($,.RADIAN.)
);
#10023=(
NAMED_UNIT(*)
SI_UNIT($,.STERADIAN.)
SOLID_ANGLE_UNIT()
);
#10028=SHAPE_DEFINITION_REPRESENTATION(#10051,#10171);
#10051=PRODUCT_DEFINITION_SHAPE('',$,#10195);
#10171=SHAPE_REPRESENTATION('',(#5910),#10000);
#10190=PRODUCT_DEFINITION_CONTEXT('part definition',#10261,'design');
#10195=PRODUCT_DEFINITION('Bonded foot pad (1)',
'Bonded foot pad (1)',#10218,#10190);
#10218=PRODUCT_DEFINITION_FORMATION('',$,#10267);
#10261=APPLICATION_CONTEXT(
'Core Data for Automotive Mechanical Design Process');
#10262=PRODUCT_CONTEXT('part definition',#10261,'mechanical');
#10267=PRODUCT('Bonded foot pad (1)','Bonded foot pad (1)',
'Bonded foot pad (1)',(#10262));
#10335=COLOUR_RGB('Sky Blue',0.24,0.69,0.87);
#10336=FILL_AREA_STYLE_COLOUR('',#10335);
#10337=FILL_AREA_STYLE('',(#10336));
#10338=SURFACE_STYLE_FILL_AREA(#10337);
#10339=SURFACE_SIDE_STYLE('',(#10338));
#10340=SURFACE_STYLE_USAGE(.BOTH.,#10339);
#10341=PRESENTATION_STYLE_ASSIGNMENT((#10340));
ENDSEC;
END-ISO-10303-21;
